ISO-10303-21;
HEADER;
/* Generated by software containing ST-Developer
 * from STEP Tools, Inc. (www.steptools.com) 
 */

FILE_DESCRIPTION(
/* description */ ('Bin tilter linkage'),
/* implementation_level */ '2;1');

FILE_NAME(
/* name */ 'Bearing cap (3).step',
/* time_stamp */ '2026-10-28T03:26:24-07:00',
/* author */ (''),
/* organization */ (''),
/* preprocessor_version */ 'ST-DEVELOPER v20.2',
/* originating_system */ 'Autodesk Translation Framework v15.17.0.0',
/* authorisation */ '');

FILE_SCHEMA (('AUTOMOTIVE_DESIGN { 1 0 10303 214 3 1 1 }'));
ENDSEC;

DATA;
#10=MECHANICAL_DESIGN_GEOMETRIC_PRESENTATION_REPRESENTATION('',(#908),#23728);
#696=SHAPE_REPRESENTATION_RELATIONSHIP('SRR','None',#24161,#802);
#802=ADVANCED_BREP_SHAPE_REPRESENTATION('',(#1021),#23661);
#908=STYLED_ITEM('',(#24765),#1021);
#1021=MANIFOLD_SOLID_BREP('Body1',#12439);
#1296=FACE_BOUND('',#3232,.T.);
#1297=FACE_BOUND('',#3233,.T.);
#1298=FACE_BOUND('',#3234,.T.);
#1299=FACE_BOUND('',#3235,.T.);
#1300=FACE_BOUND('',#3236,.T.);
#1301=FACE_BOUND('',#3238,.T.);
#1302=FACE_BOUND('',#3239,.T.);
#1303=FACE_BOUND('',#3240,.T.);
#1304=FACE_BOUND('',#3241,.T.);
#1305=FACE_BOUND('',#3242,.T.);
#1663=PLANE('',#14445);
#1664=PLANE('',#14446);
#2239=FACE_OUTER_BOUND('',#3225,.T.);
#2240=FACE_OUTER_BOUND('',#3226,.T.);
#2241=FACE_OUTER_BOUND('',#3227,.T.);
#2242=FACE_OUTER_BOUND('',#3228,.T.);
#2243=FACE_OUTER_BOUND('',#3229,.T.);
#2244=FACE_OUTER_BOUND('',#3230,.T.);
#2245=FACE_OUTER_BOUND('',#3231,.T.);
#2246=FACE_OUTER_BOUND('',#3237,.T.);
#3225=EDGE_LOOP('',(#9709,#9710,#9711,#9712));
#3226=EDGE_LOOP('',(#9713,#9714,#9715,#9716));
#3227=EDGE_LOOP('',(#9717,#9718,#9719,#9720));
#3228=EDGE_LOOP('',(#9721,#9722,#9723,#9724));
#3229=EDGE_LOOP('',(#9725,#9726,#9727,#9728));
#3230=EDGE_LOOP('',(#9729,#9730,#9731,#9732));
#3231=EDGE_LOOP('',(#9733));
#3232=EDGE_LOOP('',(#9734));
#3233=EDGE_LOOP('',(#9735));
#3234=EDGE_LOOP('',(#9736));
#3235=EDGE_LOOP('',(#9737));
#3236=EDGE_LOOP('',(#9738));
#3237=EDGE_LOOP('',(#9739));
#3238=EDGE_LOOP('',(#9740));
#3239=EDGE_LOOP('',(#9741));
#3240=EDGE_LOOP('',(#9742));
#3241=EDGE_LOOP('',(#9743));
#3242=EDGE_LOOP('',(#9744));
#4165=LINE('',#21260,#4840);
#4166=LINE('',#21266,#4841);
#4167=LINE('',#21272,#4842);
#4168=LINE('',#21278,#4843);
#4169=LINE('',#21284,#4844);
#4170=LINE('',#21290,#4845);
#4840=VECTOR('',#17296,0.225);
#4841=VECTOR('',#17303,0.225);
#4842=VECTOR('',#17310,0.225);
#4843=VECTOR('',#17317,0.225);
#4844=VECTOR('',#17324,1.02);
#4845=VECTOR('',#17331,2.2);
#5551=CIRCLE('',#14428,0.225);
#5552=CIRCLE('',#14429,0.225);
#5553=CIRCLE('',#14431,0.225);
#5554=CIRCLE('',#14432,0.225);
#5555=CIRCLE('',#14434,0.225);
#5556=CIRCLE('',#14435,0.225);
#5557=CIRCLE('',#14437,0.225);
#5558=CIRCLE('',#14438,0.225);
#5559=CIRCLE('',#14440,1.02);
#5560=CIRCLE('',#14441,1.02);
#5561=CIRCLE('',#14443,2.2);
#5562=CIRCLE('',#14444,2.2);
#6401=VERTEX_POINT('',#21257);
#6402=VERTEX_POINT('',#21259);
#6403=VERTEX_POINT('',#21263);
#6404=VERTEX_POINT('',#21265);
#6405=VERTEX_POINT('',#21269);
#6406=VERTEX_POINT('',#21271);
#6407=VERTEX_POINT('',#21275);
#6408=VERTEX_POINT('',#21277);
#6409=VERTEX_POINT('',#21281);
#6410=VERTEX_POINT('',#21283);
#6411=VERTEX_POINT('',#21287);
#6412=VERTEX_POINT('',#21289);
#7594=EDGE_CURVE('',#6401,#6401,#5551,.T.);
#7595=EDGE_CURVE('',#6401,#6402,#4165,.T.);
#7596=EDGE_CURVE('',#6402,#6402,#5552,.T.);
#7597=EDGE_CURVE('',#6403,#6403,#5553,.T.);
#7598=EDGE_CURVE('',#6403,#6404,#4166,.T.);
#7599=EDGE_CURVE('',#6404,#6404,#5554,.T.);
#7600=EDGE_CURVE('',#6405,#6405,#5555,.T.);
#7601=EDGE_CURVE('',#6405,#6406,#4167,.T.);
#7602=EDGE_CURVE('',#6406,#6406,#5556,.T.);
#7603=EDGE_CURVE('',#6407,#6407,#5557,.T.);
#7604=EDGE_CURVE('',#6407,#6408,#4168,.T.);
#7605=EDGE_CURVE('',#6408,#6408,#5558,.T.);
#7606=EDGE_CURVE('',#6409,#6409,#5559,.T.);
#7607=EDGE_CURVE('',#6409,#6410,#4169,.T.);
#7608=EDGE_CURVE('',#6410,#6410,#5560,.T.);
#7609=EDGE_CURVE('',#6411,#6411,#5561,.T.);
#7610=EDGE_CURVE('',#6411,#6412,#4170,.T.);
#7611=EDGE_CURVE('',#6412,#6412,#5562,.T.);
#9709=ORIENTED_EDGE('',*,*,#7594,.F.);
#9710=ORIENTED_EDGE('',*,*,#7595,.T.);
#9711=ORIENTED_EDGE('',*,*,#7596,.F.);
#9712=ORIENTED_EDGE('',*,*,#7595,.F.);
#9713=ORIENTED_EDGE('',*,*,#7597,.F.);
#9714=ORIENTED_EDGE('',*,*,#7598,.T.);
#9715=ORIENTED_EDGE('',*,*,#7599,.F.);
#9716=ORIENTED_EDGE('',*,*,#7598,.F.);
#9717=ORIENTED_EDGE('',*,*,#7600,.F.);
#9718=ORIENTED_EDGE('',*,*,#7601,.T.);
#9719=ORIENTED_EDGE('',*,*,#7602,.F.);
#9720=ORIENTED_EDGE('',*,*,#7601,.F.);
#9721=ORIENTED_EDGE('',*,*,#7603,.F.);
#9722=ORIENTED_EDGE('',*,*,#7604,.T.);
#9723=ORIENTED_EDGE('',*,*,#7605,.F.);
#9724=ORIENTED_EDGE('',*,*,#7604,.F.);
#9725=ORIENTED_EDGE('',*,*,#7606,.F.);
#9726=ORIENTED_EDGE('',*,*,#7607,.T.);
#9727=ORIENTED_EDGE('',*,*,#7608,.T.);
#9728=ORIENTED_EDGE('',*,*,#7607,.F.);
#9729=ORIENTED_EDGE('',*,*,#7609,.F.);
#9730=ORIENTED_EDGE('',*,*,#7610,.T.);
#9731=ORIENTED_EDGE('',*,*,#7611,.T.);
#9732=ORIENTED_EDGE('',*,*,#7610,.F.);
#9733=ORIENTED_EDGE('',*,*,#7609,.T.);
#9734=ORIENTED_EDGE('',*,*,#7606,.T.);
#9735=ORIENTED_EDGE('',*,*,#7605,.T.);
#9736=ORIENTED_EDGE('',*,*,#7602,.T.);
#9737=ORIENTED_EDGE('',*,*,#7599,.T.);
#9738=ORIENTED_EDGE('',*,*,#7596,.T.);
#9739=ORIENTED_EDGE('',*,*,#7611,.F.);
#9740=ORIENTED_EDGE('',*,*,#7608,.F.);
#9741=ORIENTED_EDGE('',*,*,#7603,.T.);
#9742=ORIENTED_EDGE('',*,*,#7600,.T.);
#9743=ORIENTED_EDGE('',*,*,#7597,.T.);
#9744=ORIENTED_EDGE('',*,*,#7594,.T.);
#11441=CYLINDRICAL_SURFACE('',#14427,0.225);
#11442=CYLINDRICAL_SURFACE('',#14430,0.225);
#11443=CYLINDRICAL_SURFACE('',#14433,0.225);
#11444=CYLINDRICAL_SURFACE('',#14436,0.225);
#11445=CYLINDRICAL_SURFACE('',#14439,1.02);
#11446=CYLINDRICAL_SURFACE('',#14442,2.2);
#11964=ADVANCED_FACE('',(#2239),#11441,.F.);
#11965=ADVANCED_FACE('',(#2240),#11442,.F.);
#11966=ADVANCED_FACE('',(#2241),#11443,.F.);
#11967=ADVANCED_FACE('',(#2242),#11444,.F.);
#11968=ADVANCED_FACE('',(#2243),#11445,.F.);
#11969=ADVANCED_FACE('',(#2244),#11446,.T.);
#11970=ADVANCED_FACE('',(#2245,#1296,#1297,#1298,#1299,#1300),#1663,.T.);
#11971=ADVANCED_FACE('',(#2246,#1301,#1302,#1303,#1304,#1305),#1664,.F.);
#12439=CLOSED_SHELL('',(#11964,#11965,#11966,#11967,#11968,#11969,#11970,
#11971));
#14426=AXIS2_PLACEMENT_3D('',#21255,#17290,#17291);
#14427=AXIS2_PLACEMENT_3D('',#21256,#17292,#17293);
#14428=AXIS2_PLACEMENT_3D('',#21258,#17294,#17295);
#14429=AXIS2_PLACEMENT_3D('',#21261,#17297,#17298);
#14430=AXIS2_PLACEMENT_3D('',#21262,#17299,#17300);
#14431=AXIS2_PLACEMENT_3D('',#21264,#17301,#17302);
#14432=AXIS2_PLACEMENT_3D('',#21267,#17304,#17305);
#14433=AXIS2_PLACEMENT_3D('',#21268,#17306,#17307);
#14434=AXIS2_PLACEMENT_3D('',#21270,#17308,#17309);
#14435=AXIS2_PLACEMENT_3D('',#21273,#17311,#17312);
#14436=AXIS2_PLACEMENT_3D('',#21274,#17313,#17314);
#14437=AXIS2_PLACEMENT_3D('',#21276,#17315,#17316);
#14438=AXIS2_PLACEMENT_3D('',#21279,#17318,#17319);
#14439=AXIS2_PLACEMENT_3D('',#21280,#17320,#17321);
#14440=AXIS2_PLACEMENT_3D('',#21282,#17322,#17323);
#14441=AXIS2_PLACEMENT_3D('',#21285,#17325,#17326);
#14442=AXIS2_PLACEMENT_3D('',#21286,#17327,#17328);
#14443=AXIS2_PLACEMENT_3D('',#21288,#17329,#17330);
#14444=AXIS2_PLACEMENT_3D('',#21291,#17332,#17333);
#14445=AXIS2_PLACEMENT_3D('',#21292,#17334,#17335);
#14446=AXIS2_PLACEMENT_3D('',#21293,#17336,#17337);
#17290=DIRECTION('axis',(0.,0.,1.));
#17291=DIRECTION('refdir',(1.,0.,0.));
#17292=DIRECTION('center_axis',(0.,1.,0.));
#17293=DIRECTION('ref_axis',(1.,0.,0.));
#17294=DIRECTION('center_axis',(0.,1.,0.));
#17295=DIRECTION('ref_axis',(1.,0.,0.));
#17296=DIRECTION('',(0.,1.,0.));
#17297=DIRECTION('center_axis',(0.,-1.,0.));
#17298=DIRECTION('ref_axis',(1.,0.,0.));
#17299=DIRECTION('center_axis',(0.,1.,0.));
#17300=DIRECTION('ref_axis',(1.,0.,0.));
#17301=DIRECTION('center_axis',(0.,1.,0.));
#17302=DIRECTION('ref_axis',(1.,0.,0.));
#17303=DIRECTION('',(0.,1.,0.));
#17304=DIRECTION('center_axis',(0.,-1.,0.));
#17305=DIRECTION('ref_axis',(1.,0.,0.));
#17306=DIRECTION('center_axis',(0.,1.,0.));
#17307=DIRECTION('ref_axis',(1.,0.,0.));
#17308=DIRECTION('center_axis',(0.,1.,0.));
#17309=DIRECTION('ref_axis',(1.,0.,0.));
#17310=DIRECTION('',(0.,1.,0.));
#17311=DIRECTION('center_axis',(0.,-1.,0.));
#17312=DIRECTION('ref_axis',(1.,0.,0.));
#17313=DIRECTION('center_axis',(0.,1.,0.));
#17314=DIRECTION('ref_axis',(1.,0.,0.));
#17315=DIRECTION('center_axis',(0.,1.,0.));
#17316=DIRECTION('ref_axis',(1.,0.,0.));
#17317=DIRECTION('',(0.,1.,0.));
#17318=DIRECTION('center_axis',(0.,-1.,0.));
#17319=DIRECTION('ref_axis',(1.,0.,0.));
#17320=DIRECTION('center_axis',(0.,1.,0.));
#17321=DIRECTION('ref_axis',(1.,0.,0.));
#17322=DIRECTION('center_axis',(0.,-1.,0.));
#17323=DIRECTION('ref_axis',(1.,0.,0.));
#17324=DIRECTION('',(0.,-1.,0.));
#17325=DIRECTION('center_axis',(0.,-1.,0.));
#17326=DIRECTION('ref_axis',(1.,0.,0.));
#17327=DIRECTION('center_axis',(0.,1.,0.));
#17328=DIRECTION('ref_axis',(1.,0.,0.));
#17329=DIRECTION('center_axis',(0.,1.,0.));
#17330=DIRECTION('ref_axis',(1.,0.,0.));
#17331=DIRECTION('',(0.,-1.,0.));
#17332=DIRECTION('center_axis',(0.,1.,0.));
#17333=DIRECTION('ref_axis',(1.,0.,0.));
#17334=DIRECTION('center_axis',(0.,1.,0.));
#17335=DIRECTION('ref_axis',(1.,0.,0.));
#17336=DIRECTION('center_axis',(0.,1.,0.));
#17337=DIRECTION('ref_axis',(1.,0.,0.));
#21255=CARTESIAN_POINT('',(0.,0.,0.));
#21256=CARTESIAN_POINT('Origin',(8.08877866266397,0.4,17.1120538880616));
#21257=CARTESIAN_POINT('',(7.86377866266397,0.5,17.1120538880616));
#21258=CARTESIAN_POINT('Origin',(8.08877866266397,0.5,17.1120538880616));
#21259=CARTESIAN_POINT('',(7.86377866266397,0.8,17.1120538880616));
#21260=CARTESIAN_POINT('',(7.86377866266397,0.4,17.1120538880616));
#21261=CARTESIAN_POINT('Origin',(8.08877866266397,0.8,17.1120538880616));
#21262=CARTESIAN_POINT('Origin',(8.08877866266397,0.4,19.7283489784518));
#21263=CARTESIAN_POINT('',(7.86377866266397,0.5,19.7283489784518));
#21264=CARTESIAN_POINT('Origin',(8.08877866266397,0.5,19.7283489784518));
#21265=CARTESIAN_POINT('',(7.86377866266397,0.8,19.7283489784518));
#21266=CARTESIAN_POINT('',(7.86377866266397,0.4,19.7283489784518));
#21267=CARTESIAN_POINT('Origin',(8.08877866266397,0.8,19.7283489784518));
#21268=CARTESIAN_POINT('Origin',(10.7050737530542,0.4,19.7283489784518));
#21269=CARTESIAN_POINT('',(10.4800737530542,0.5,19.7283489784518));
#21270=CARTESIAN_POINT('Origin',(10.7050737530542,0.5,19.7283489784518));
#21271=CARTESIAN_POINT('',(10.4800737530542,0.8,19.7283489784518));
#21272=CARTESIAN_POINT('',(10.4800737530542,0.4,19.7283489784518));
#21273=CARTESIAN_POINT('Origin',(10.7050737530542,0.8,19.7283489784518));
#21274=CARTESIAN_POINT('Origin',(10.7050737530542,0.4,17.1120538880616));
#21275=CARTESIAN_POINT('',(10.4800737530542,0.5,17.1120538880616));
#21276=CARTESIAN_POINT('Origin',(10.7050737530542,0.5,17.1120538880616));
#21277=CARTESIAN_POINT('',(10.4800737530542,0.8,17.1120538880616));
#21278=CARTESIAN_POINT('',(10.4800737530542,0.4,17.1120538880616));
#21279=CARTESIAN_POINT('Origin',(10.7050737530542,0.8,17.1120538880616));
#21280=CARTESIAN_POINT('Origin',(9.39692620785909,0.5,18.4202014332567));
#21281=CARTESIAN_POINT('',(8.37692620785909,0.8,18.4202014332567));
#21282=CARTESIAN_POINT('Origin',(9.39692620785909,0.8,18.4202014332567));
#21283=CARTESIAN_POINT('',(8.37692620785909,0.5,18.4202014332567));
#21284=CARTESIAN_POINT('',(8.37692620785909,0.5,18.4202014332567));
#21285=CARTESIAN_POINT('Origin',(9.39692620785909,0.5,18.4202014332567));
#21286=CARTESIAN_POINT('Origin',(9.39692620785909,0.5,18.4202014332567));
#21287=CARTESIAN_POINT('',(7.19692620785909,0.8,18.4202014332567));
#21288=CARTESIAN_POINT('Origin',(9.39692620785909,0.8,18.4202014332567));
#21289=CARTESIAN_POINT('',(7.19692620785909,0.5,18.4202014332567));
#21290=CARTESIAN_POINT('',(7.19692620785909,0.5,18.4202014332567));
#21291=CARTESIAN_POINT('Origin',(9.39692620785909,0.5,18.4202014332567));
#21292=CARTESIAN_POINT('Origin',(9.39692620785909,0.8,18.4202014332567));
#21293=CARTESIAN_POINT('Origin',(9.39692620785909,0.5,18.4202014332567));
#23544=UNCERTAINTY_MEASURE_WITH_UNIT(LENGTH_MEASURE(0.001),#23729,
'DISTANCE_ACCURACY_VALUE',
'Maximum model space distance between geometric entities at asserted c
onnectivities');
#23611=UNCERTAINTY_MEASURE_WITH_UNIT(LENGTH_MEASURE(0.001),#23729,
'DISTANCE_ACCURACY_VALUE',
'Maximum model space distance between geometric entities at asserted c
onnectivities');
#23661=(
GEOMETRIC_REPRESENTATION_CONTEXT(3)
GLOBAL_UNCERTAINTY_ASSIGNED_CONTEXT((#23544))
GLOBAL_UNIT_ASSIGNED_CONTEXT((#23729,#23731,#23732))
REPRESENTATION_CONTEXT('','3D')
);
#23728=(
GEOMETRIC_REPRESENTATION_CONTEXT(3)
GLOBAL_UNCERTAINTY_ASSIGNED_CONTEXT((#23611))
GLOBAL_UNIT_ASSIGNED_CONTEXT((#23729,#23731,#23732))
REPRESENTATION_CONTEXT('','3D')
);
#23729=(
LENGTH_UNIT()
NAMED_UNIT(*)
SI_UNIT(.CENTI.,.METRE.)
);
#23731=(
NAMED_UNIT(*)
PLANE_ANGLE_UNIT()
SI_UNIT($,.RADIAN.)
);
#23732=(
NAMED_UNIT(*)
SI_UNIT($,.STERADIAN.)
SOLID_ANGLE_UNIT()
);
#23782=SHAPE_DEFINITION_REPRESENTATION(#23898,#24161);
#23898=PRODUCT_DEFINITION_SHAPE('',$,#24278);
#24161=SHAPE_REPRESENTATION('',(#14426),#23661);
#24228=PRODUCT_DEFINITION_CONTEXT('part definition',#24578,'design');
#24278=PRODUCT_DEFINITION('Bearing cap (3)','Bearing cap (3)',#24394,#24228);
#24394=PRODUCT_DEFINITION_FORMATION('',$,#24629);
#24578=APPLICATION_CONTEXT(
'Core Data for Automotive Mechanical Design Process');
#24579=PRODUCT_CONTEXT('part definition',#24578,'mechanical');
#24629=PRODUCT('Bearing cap (3)','Bearing cap (3)','Bearing cap (3)',(#24579));
#24759=COLOUR_RGB('Grey',0.48,0.52,0.57);
#24760=FILL_AREA_STYLE_COLOUR('',#24759);
#24761=FILL_AREA_STYLE('',(#24760));
#24762=SURFACE_STYLE_FILL_AREA(#24761);
#24763=SURFACE_SIDE_STYLE('',(#24762));
#24764=SURFACE_STYLE_USAGE(.BOTH.,#24763);
#24765=PRESENTATION_STYLE_ASSIGNMENT((#24764));
ENDSEC;
END-ISO-10303-21;
